ISO-10303-21;
HEADER;
/* Generated by software containing ST-Developer
 * from STEP Tools, Inc. (www.steptools.com) 
 */

FILE_DESCRIPTION(
/* description */ ('Indexing fixture plate with plunger'),
/* implementation_level */ '2;1');

FILE_NAME(
/* name */ 'Bonded foot (1).step',
/* time_stamp */ '2026-10-28T03:23:41-07:00',
/* author */ (''),
/* organization */ (''),
/* preprocessor_version */ 'ST-DEVELOPER v20.2',
/* originating_system */ 'Autodesk Translation Framework v15.17.0.0',
/* authorisation */ '');

FILE_SCHEMA (('AUTOMOTIVE_DESIGN { 1 0 10303 214 3 1 1 }'));
ENDSEC;

DATA;
#10=MECHANICAL_DESIGN_GEOMETRIC_PRESENTATION_REPRESENTATION('',(#319),#10020);
#265=SHAPE_REPRESENTATION_RELATIONSHIP('SRR','None',#10139,#292);
#292=ADVANCED_BREP_SHAPE_REPRESENTATION('',(#355),#9992);
#319=STYLED_ITEM('',(#10382),#355);
#355=MANIFOLD_SOLID_BREP('Body1',#4573);
#545=PLANE('',#4947);
#546=PLANE('',#4948);
#686=FACE_OUTER_BOUND('',#986,.T.);
#687=FACE_OUTER_BOUND('',#987,.T.);
#688=FACE_OUTER_BOUND('',#988,.T.);
#986=EDGE_LOOP('',(#3135,#3136,#3137,#3138));
#987=EDGE_LOOP('',(#3139));
#988=EDGE_LOOP('',(#3140));
#1412=LINE('',#7210,#1632);
#1632=VECTOR('',#5671,1.);
#1848=CIRCLE('',#4945,1.);
#1849=CIRCLE('',#4946,1.);
#2159=VERTEX_POINT('',#7207);
#2160=VERTEX_POINT('',#7209);
#2547=EDGE_CURVE('',#2159,#2159,#1848,.T.);
#2548=EDGE_CURVE('',#2159,#2160,#1412,.T.);
#2549=EDGE_CURVE('',#2160,#2160,#1849,.T.);
#3135=ORIENTED_EDGE('',*,*,#2547,.F.);
#3136=ORIENTED_EDGE('',*,*,#2548,.T.);
#3137=ORIENTED_EDGE('',*,*,#2549,.T.);
#3138=ORIENTED_EDGE('',*,*,#2548,.F.);
#3139=ORIENTED_EDGE('',*,*,#2547,.T.);
#3140=ORIENTED_EDGE('',*,*,#2549,.F.);
#4175=CYLINDRICAL_SURFACE('',#4944,1.);
#4301=ADVANCED_FACE('',(#686),#4175,.T.);
#4302=ADVANCED_FACE('',(#687),#545,.T.);
#4303=ADVANCED_FACE('',(#688),#546,.F.);
#4573=CLOSED_SHELL('',(#4301,#4302,#4303));
#4943=AXIS2_PLACEMENT_3D('',#7205,#5665,#5666);
#4944=AXIS2_PLACEMENT_3D('',#7206,#5667,#5668);
#4945=AXIS2_PLACEMENT_3D('',#7208,#5669,#5670);
#4946=AXIS2_PLACEMENT_3D('',#7211,#5672,#5673);
#4947=AXIS2_PLACEMENT_3D('',#7212,#5674,#5675);
#4948=AXIS2_PLACEMENT_3D('',#7213,#5676,#5677);
#5665=DIRECTION('axis',(0.,0.,1.));
#5666=DIRECTION('refdir',(1.,0.,0.));
#5667=DIRECTION('center_axis',(0.,0.,1.));
#5668=DIRECTION('ref_axis',(1.,0.,0.));
#5669=DIRECTION('center_axis',(0.,0.,1.));
#5670=DIRECTION('ref_axis',(1.,0.,0.));
#5671=DIRECTION('',(0.,0.,-1.));
#5672=DIRECTION('center_axis',(0.,0.,1.));
#5673=DIRECTION('ref_axis',(1.,0.,0.));
#5674=DIRECTION('center_axis',(0.,0.,1.));
#5675=DIRECTION('ref_axis',(1.,0.,0.));
#5676=DIRECTION('center_axis',(0.,0.,1.));
#5677=DIRECTION('ref_axis',(1.,0.,0.));
#7205=CARTESIAN_POINT('',(0.,0.,0.));
#7206=CARTESIAN_POINT('Origin',(-9.5,9.5,-3.5));
#7207=CARTESIAN_POINT('',(-10.5,9.5,-1.));
#7208=CARTESIAN_POINT('Origin',(-9.5,9.5,-1.));
#7209=CARTESIAN_POINT('',(-10.5,9.5,-3.5));
#7210=CARTESIAN_POINT('',(-10.5,9.5,-3.5));
#7211=CARTESIAN_POINT('Origin',(-9.5,9.5,-3.5));
#7212=CARTESIAN_POINT('Origin',(-9.5,9.5,-1.));
#7213=CARTESIAN_POINT('Origin',(-9.5,9.5,-3.5));
#9959=UNCERTAINTY_MEASURE_WITH_UNIT(LENGTH_MEASURE(0.001),#10021,
'DISTANCE_ACCURACY_VALUE',
'Maximum model space distance between geometric entities at asserted c
onnectivities');
#9987=UNCERTAINTY_MEASURE_WITH_UNIT(LENGTH_MEASURE(0.001),#10021,
'DISTANCE_ACCURACY_VALUE',
'Maximum model space distance between geometric entities at asserted c
onnectivities');
#9992=(
GEOMETRIC_REPRESENTATION_CONTEXT(3)
GLOBAL_UNCERTAINTY_ASSIGNED_CONTEXT((#9959))
GLOBAL_UNIT_ASSIGNED_CONTEXT((#10021,#10023,#10024))
REPRESENTATION_CONTEXT('','3D')
);
#10020=(
GEOMETRIC_REPRESENTATION_CONTEXT(3)
GLOBAL_UNCERTAINTY_ASSIGNED_CONTEXT((#9987))
GLOBAL_UNIT_ASSIGNED_CONTEXT((#10021,#10023,#10024))
REPRESENTATION_CONTEXT('','3D')
);
#10021=(
LENGTH_UNIT()
NAMED_UNIT(*)
SI_UNIT(.CENTI.,.METRE.)
);
#10023=(
NAMED_UNIT(*)
PLANE_ANGLE_UNIT()
SI_UNIT($,.RADIAN.)
);
#10024=(
NAMED_UNIT(*)
SI_UNIT($,.STERADIAN.)
SOLID_ANGLE_UNIT()
);
#10029=SHAPE_DEFINITION_REPRESENTATION(#10061,#10139);
#10061=PRODUCT_DEFINITION_SHAPE('',$,#10172);
#10139=SHAPE_REPRESENTATION('',(#4943),#9992);
#10167=PRODUCT_DEFINITION_CONTEXT('part definition',#10265,'design');
#10172=PRODUCT_DEFINITION('Bonded foot (1)','Bonded foot (1)',#10204,#10167);
#10204=PRODUCT_DEFINITION_FORMATION('',$,#10271);
#10265=APPLICATION_CONTEXT(
'Core Data for Automotive Mechanical Design Process');
#10266=PRODUCT_CONTEXT('part definition',#10265,'mechanical');
#10271=PRODUCT('Bonded foot (1)','Bonded foot (1)','Bonded foot (1)',(#10266));
#10376=COLOUR_RGB('Off White',0.89,0.88,0.83);
#10377=FILL_AREA_STYLE_COLOUR('',#10376);
#10378=FILL_AREA_STYLE('',(#10377));
#10379=SURFACE_STYLE_FILL_AREA(#10378);
#10380=SURFACE_SIDE_STYLE('',(#10379));
#10381=SURFACE_STYLE_USAGE(.BOTH.,#10380);
#10382=PRESENTATION_STYLE_ASSIGNMENT((#10381));
ENDSEC;
END-ISO-10303-21;
